ISO-10303-21;
HEADER;
FILE_DESCRIPTION (('STEP AP214'),
    '1' );
FILE_NAME ('socket head cap screw_iso_ISO 4762 M12 x 20 - 20N.step',
    '2026-10-19T17:36:30',
    ( '' ),
    ( '' ),
    'SwSTEP 2.0',
    'SolidWorks 2025',
    '' );
FILE_SCHEMA (( 'AUTOMOTIVE_DESIGN' ));
ENDSEC;

DATA;
#8=PRODUCT ( 'socket head cap screw_iso_ISO 4762 M12 x 20 - 20N', 'socket head cap screw_iso_ISO 4762 M12 x 20 - 20N', '', ( #2148 ) ) ;
#15=AXIS2_PLACEMENT_3D ( 'NONE', #3653, #6573, #1689 ) ;
#47=ORIENTED_EDGE ( 'NONE', *, *, #4033, .T. ) ;
#108=CYLINDRICAL_SURFACE ( 'NONE', #8780, 6.000000000000003553 ) ;
#121=DIRECTION ( 'NONE',  ( 0.000000000000000000, -1.000000000000000000, 1.039664082171044481E-15 ) ) ;
#124=AXIS2_PLACEMENT_3D ( 'NONE', #8869, #5257, #7026 ) ;
#127=PLANE ( 'NONE',  #5041 ) ;
#158=ORIENTED_EDGE ( 'NONE', *, *, #6876, .T. ) ;
#161=CONICAL_SURFACE ( 'NONE', #12112, 5.057500000000000107, 1.047197551196592302 ) ;
#170=CARTESIAN_POINT ( 'NONE',  ( -31.74999999999995737, 0.000000000000000000, 0.000000000000000000 ) ) ;
#191=DIRECTION ( 'NONE',  ( -1.000000000000000000, 0.000000000000000000, -0.000000000000000000 ) ) ;
#207=DIRECTION ( 'NONE',  ( 1.000000000000000000, 0.000000000000000000, 0.000000000000000000 ) ) ;
#245=LINE ( 'NONE', #7790, #3780 ) ;
#248=CARTESIAN_POINT ( 'NONE',  ( 31.03600000000003689, 0.000000000000000000, 6.000000000000003553 ) ) ;
#255=ADVANCED_FACE ( 'NONE', ( #3893 ), #3702, .T. ) ;
#267=CARTESIAN_POINT ( 'NONE',  ( 6.000000000000000000, -2.919948986426538884, -5.057499999999997442 ) ) ;
#278=ORIENTED_EDGE ( 'NONE', *, *, #319, .T. ) ;
#296=ORIENTED_EDGE ( 'NONE', *, *, #3871, .F. ) ;
#311=PLANE ( 'NONE',  #124 ) ;
#319=EDGE_CURVE ( 'NONE', #2922, #1223, #6665, .T. ) ;
#324=DIRECTION ( 'NONE',  ( -1.000000000000000000, -0.000000000000000000, -0.000000000000000000 ) ) ;
#347=DIRECTION ( 'NONE',  ( 0.000000000000000000, 1.000000000000000000, -1.336710962791342904E-15 ) ) ;
#371=DIRECTION ( 'NONE',  ( 1.000000000000000000, 0.000000000000000000, 0.000000000000000000 ) ) ;
#399=CARTESIAN_POINT ( 'NONE',  ( 6.000000000000000000, -5.839897972853063557, 6.938893903907228378E-15 ) ) ;
#413=AXIS2_PLACEMENT_3D ( 'NONE', #7308, #9161, #9285 ) ;
#420=EDGE_LOOP ( 'NONE', ( #3998, #9368 ) ) ;
#425=AXIS2_PLACEMENT_3D ( 'NONE', #10021, #6087, #1331 ) ;
#457=( NAMED_UNIT ( * ) SI_UNIT ( $, .STERADIAN. ) SOLID_ANGLE_UNIT ( ) );
#459=DIRECTION ( 'NONE',  ( 1.000000000000000000, 0.000000000000000000, 0.000000000000000000 ) ) ;
#466=CARTESIAN_POINT ( 'NONE',  ( 32.00000000000000000, 6.167321280506070407E-16, -5.035999999999999588 ) ) ;
#478=AXIS2_PLACEMENT_3D ( 'NONE', #3709, #6569, #4544 ) ;
#498=EDGE_CURVE ( 'NONE', #1359, #6574, #5547, .T. ) ;
#505=CARTESIAN_POINT ( 'NONE',  ( 12.59999999999999964, 0.000000000000000000, 0.000000000000000000 ) ) ;
#507=CARTESIAN_POINT ( 'NONE',  ( 0.000000000000000000, 0.000000000000000000, 0.000000000000000000 ) ) ;
#520=FACE_OUTER_BOUND ( 'NONE', #7436, .T. ) ;
#552=CARTESIAN_POINT ( 'NONE',  ( 12.59999999999999964, 0.000000000000000000, -6.600000000000003197 ) ) ;
#577=AXIS2_PLACEMENT_3D ( 'NONE', #5068, #2970, #6082 ) ;
#588=LINE ( 'NONE', #9035, #618 ) ;
#618=VECTOR ( 'NONE', #347, 1000.000000000000000 ) ;
#620=CARTESIAN_POINT ( 'NONE',  ( 31.03600000000003689, 0.000000000000000000, 0.000000000000000000 ) ) ;
#634=AXIS2_PLACEMENT_3D ( 'NONE', #11656, #12414, #9926 ) ;
#679=ADVANCED_FACE ( 'NONE', ( #6727, #838 ), #7692, .T. ) ;
#708=( GEOMETRIC_REPRESENTATION_CONTEXT ( 3 ) GLOBAL_UNCERTAINTY_ASSIGNED_CONTEXT ( ( #3862 ) ) GLOBAL_UNIT_ASSIGNED_CONTEXT ( ( #7814, #3430, #457 ) ) REPRESENTATION_CONTEXT ( 'NONE', 'WORKASPACE' ) );
#736=CARTESIAN_POINT ( 'NONE',  ( 6.000000000000000000, 2.919948986426526005, -5.057500000000003659 ) ) ;
#757=DIRECTION ( 'NONE',  ( 0.000000000000000000, 0.4999999999999987232, -0.8660254037844393737 ) ) ;
#770=ORIENTED_EDGE ( 'NONE', *, *, #11974, .F. ) ;
#801=VERTEX_POINT ( 'NONE', #9024 ) ;
#826=CIRCLE ( 'NONE', #8942, 0.5999999999999998668 ) ;
#836=ORIENTED_EDGE ( 'NONE', *, *, #10882, .F. ) ;
#838=FACE_OUTER_BOUND ( 'NONE', #10049, .T. ) ;
#885=AXIS2_PLACEMENT_3D ( 'NONE', #7770, #5047, #2950 ) ;
#895=ORIENTED_EDGE ( 'NONE', *, *, #10610, .T. ) ;
#905=EDGE_CURVE ( 'NONE', #2831, #5337, #9640, .T. ) ;
#921=ORIENTED_EDGE ( 'NONE', *, *, #7265, .F. ) ;
#929=ORIENTED_EDGE ( 'NONE', *, *, #9179, .F. ) ;
#932=LINE ( 'NONE', #8664, #7977 ) ;
#934=EDGE_LOOP ( 'NONE', ( #7388, #10470, #4956, #11399 ) ) ;
#936=DIRECTION ( 'NONE',  ( -1.000000000000000000, -0.000000000000000000, -0.000000000000000000 ) ) ;
#944=CARTESIAN_POINT ( 'NONE',  ( 11.99999999999999822, 0.000000000000000000, 0.000000000000000000 ) ) ;
#954=AXIS2_PLACEMENT_3D ( 'NONE', #4744, #1752, #9509 ) ;
#979=CARTESIAN_POINT ( 'NONE',  ( 6.000000000000000000, 8.759846959279592227, -5.057500000000009877 ) ) ;
#1000=DIRECTION ( 'NONE',  ( 0.000000000000000000, 0.000000000000000000, 1.000000000000000000 ) ) ;
#1004=ADVANCED_FACE ( 'NONE', ( #4240 ), #311, .F. ) ;
#1013=FACE_OUTER_BOUND ( 'NONE', #6745, .T. ) ;
#1036=DIRECTION ( 'NONE',  ( 0.000000000000000000, 0.000000000000000000, 1.000000000000000000 ) ) ;
#1119=DIRECTION ( 'NONE',  ( -1.000000000000000000, -0.000000000000000000, -0.000000000000000000 ) ) ;
#1129=VECTOR ( 'NONE', #1119, 1000.000000000000000 ) ;
#1139=DIRECTION ( 'NONE',  ( -1.000000000000000000, -0.000000000000000000, -0.000000000000000000 ) ) ;
#1143=ORIENTED_EDGE ( 'NONE', *, *, #10775, .T. ) ;
#1145=VECTOR ( 'NONE', #11967, 1000.000000000000000 ) ;
#1173=EDGE_LOOP ( 'NONE', ( #10670, #4078, #770, #3547 ) ) ;
#1180=VECTOR ( 'NONE', #4602, 1000.000000000000000 ) ;
#1203=CARTESIAN_POINT ( 'NONE',  ( 6.000000000000000000, 2.919948986426526005, -5.057500000000003659 ) ) ;
#1223=VERTEX_POINT ( 'NONE', #11206 ) ;
#1296=ORIENTED_EDGE ( 'NONE', *, *, #6893, .T. ) ;
#1300=ADVANCED_FACE ( 'NONE', ( #12475 ), #11868, .T. ) ;
#1316=LINE ( 'NONE', #8101, #1145 ) ;
#1330=ADVANCED_FACE ( 'NONE', ( #6825 ), #9644, .T. ) ;
#1331=DIRECTION ( 'NONE',  ( 0.000000000000000000, 0.000000000000000000, 1.000000000000000000 ) ) ;
#1359=VERTEX_POINT ( 'NONE', #5629 ) ;
#1394=EDGE_CURVE ( 'NONE', #9622, #8859, #7003, .T. ) ;
#1435=CARTESIAN_POINT ( 'NONE',  ( 6.000000000000000000, 5.839897972853065333, -6.938893903907228378E-15 ) ) ;
#1448=CARTESIAN_POINT ( 'NONE',  ( 0.6000000000000033085, 0.000000000000000000, 0.000000000000000000 ) ) ;
#1504=DIRECTION ( 'NONE',  ( 0.000000000000000000, 0.000000000000000000, -1.000000000000000000 ) ) ;
#1505=DIRECTION ( 'NONE',  ( 0.000000000000000000, 0.4999999999999987232, -0.8660254037844393737 ) ) ;
#1507=DIRECTION ( 'NONE',  ( -1.000000000000000000, -0.000000000000000000, -0.000000000000000000 ) ) ;
#1524=EDGE_CURVE ( 'NONE', #3004, #6574, #1316, .T. ) ;
#1560=VERTEX_POINT ( 'NONE', #7137 ) ;
#1588=CARTESIAN_POINT ( 'NONE',  ( 6.000000000000000000, 0.000000000000000000, 0.000000000000000000 ) ) ;
#1589=AXIS2_PLACEMENT_3D ( 'NONE', #944, #3788, #3720 ) ;
#1624=DIRECTION ( 'NONE',  ( 0.000000000000000000, 0.000000000000000000, 1.000000000000000000 ) ) ;
#1635=FACE_OUTER_BOUND ( 'NONE', #1173, .T. ) ;
#1645=VECTOR ( 'NONE', #9659, 1000.000000000000000 ) ;
#1666=PLANE ( 'NONE',  #11498 ) ;
#1674=VERTEX_POINT ( 'NONE', #12030 ) ;
#1689=DIRECTION ( 'NONE',  ( 0.000000000000000000, -0.4999999999999986677, 0.8660254037844392627 ) ) ;
#1691=PRODUCT_DEFINITION ( 'UNKNOWN', '', #9398, #9044 ) ;
#1732=CARTESIAN_POINT ( 'NONE',  ( 6.000000000000000000, -2.919948986426525117, 5.057500000000004547 ) ) ;
#1747=FACE_OUTER_BOUND ( 'NONE', #10984, .T. ) ;
#1752=DIRECTION ( 'NONE',  ( -1.000000000000000000, -0.000000000000000000, -0.000000000000000000 ) ) ;
#1785=DIRECTION ( 'NONE',  ( -0.5000000000000046629, 1.060575238724903587E-16, -0.8660254037844359321 ) ) ;
#1793=VECTOR ( 'NONE', #6505, 1000.000000000000000 ) ;
#1812=DIRECTION ( 'NONE',  ( 0.000000000000000000, 0.000000000000000000, 1.000000000000000000 ) ) ;
#1820=CARTESIAN_POINT ( 'NONE',  ( 6.000000000000000000, 6.760415694317218303E-15, 5.057500000000000995 ) ) ;
#1876=DIRECTION ( 'NONE',  ( 0.000000000000000000, 0.000000000000000000, 1.000000000000000000 ) ) ;
#1879=CIRCLE ( 'NONE', #6146, 9.000000000000000000 ) ;
#1901=CYLINDRICAL_SURFACE ( 'NONE', #10138, 6.000000000000003553 ) ;
#1902=ORIENTED_EDGE ( 'NONE', *, *, #9179, .T. ) ;
#1957=CARTESIAN_POINT ( 'NONE',  ( 0.000000000000000000, 0.000000000000000000, 0.000000000000000000 ) ) ;
#1965=ORIENTED_EDGE ( 'NONE', *, *, #9329, .T. ) ;
#1979=VERTEX_POINT ( 'NONE', #4863 ) ;
#2000=DIRECTION ( 'NONE',  ( -1.000000000000000000, -0.000000000000000000, -0.000000000000000000 ) ) ;
#2012=CARTESIAN_POINT ( 'NONE',  ( 32.00000000000000000, 0.000000000000000000, 0.000000000000000000 ) ) ;
#2015=ORIENTED_EDGE ( 'NONE', *, *, #9935, .F. ) ;
#2016=DIRECTION ( 'NONE',  ( -1.000000000000000000, -0.000000000000000000, -0.000000000000000000 ) ) ;
#2017=AXIS2_PLACEMENT_3D ( 'NONE', #2923, #8885, #8819 ) ;
#2048=AXIS2_PLACEMENT_3D ( 'NONE', #1588, #9578, #11357 ) ;
#2060=DIRECTION ( 'NONE',  ( -1.000000000000000000, -0.000000000000000000, -0.000000000000000000 ) ) ;
#2062=EDGE_CURVE ( 'NONE', #1674, #9622, #12153, .T. ) ;
#2066=ORIENTED_EDGE ( 'NONE', *, *, #319, .F. ) ;
#2079=EDGE_CURVE ( 'NONE', #9848, #8345, #9051, .T. ) ;
#2083=DIRECTION ( 'NONE',  ( 0.000000000000000000, 1.000000000000000000, -1.336710962791342904E-15 ) ) ;
#2096=ORIENTED_EDGE ( 'NONE', *, *, #11173, .T. ) ;
#2146=ORIENTED_EDGE ( 'NONE', *, *, #2414, .F. ) ;
#2148=PRODUCT_CONTEXT ( 'NONE', #9350, 'mechanical' ) ;
#2182=EDGE_LOOP ( 'NONE', ( #7575, #1902, #6930, #1965, #2594 ) ) ;
#2184=VECTOR ( 'NONE', #1785, 1000.000000000000000 ) ;
#2193=DIRECTION ( 'NONE',  ( -1.000000000000000000, -0.000000000000000000, -0.000000000000000000 ) ) ;
#2202=VERTEX_POINT ( 'NONE', #3889 ) ;
#2210=PLANE ( 'NONE',  #577 ) ;
#2279=VERTEX_POINT ( 'NONE', #10934 ) ;
#2298=EDGE_CURVE ( 'NONE', #8987, #2922, #11550, .T. ) ;
#2304=AXIS2_PLACEMENT_3D ( 'NONE', #620, #1507, #12167 ) ;
#2314=EDGE_CURVE ( 'NONE', #5337, #3004, #588, .T. ) ;
#2346=EDGE_CURVE ( 'NONE', #10081, #1979, #2366, .T. ) ;
#2357=SHAPE_REPRESENTATION_RELATIONSHIP ( 'NONE' , 'NONE' ,  #3370, #8540 ) ;
#2366=LINE ( 'NONE', #466, #3850 ) ;
#2377=DIRECTION ( 'NONE',  ( 0.000000000000000000, 1.000000000000000000, -1.336710962791342904E-15 ) ) ;
#2389=CARTESIAN_POINT ( 'NONE',  ( 6.000000000000000000, 5.839897972853065333, -6.938893903907228378E-15 ) ) ;
#2406=DIRECTION ( 'NONE',  ( -0.000000000000000000, 1.000000000000000000, 1.224646799147353207E-16 ) ) ;
#2414=EDGE_CURVE ( 'NONE', #12065, #2755, #7092, .T. ) ;
#2446=FACE_OUTER_BOUND ( 'NONE', #2182, .T. ) ;
#2452=PLANE ( 'NONE',  #4756 ) ;
#2465=DIRECTION ( 'NONE',  ( 0.000000000000000000, -1.224646799147353207E-16, 1.000000000000000000 ) ) ;
#2485=VERTEX_POINT ( 'NONE', #12198 ) ;
#2517=LINE ( 'NONE', #4483, #3135 ) ;
#2523=DIRECTION ( 'NONE',  ( 0.000000000000000000, 0.000000000000000000, -1.000000000000000000 ) ) ;
#2539=DIRECTION ( 'NONE',  ( 0.000000000000000000, -0.5000000000000011102, -0.8660254037844380415 ) ) ;
#2548=ORIENTED_EDGE ( 'NONE', *, *, #6876, .F. ) ;
#2558=VECTOR ( 'NONE', #2083, 1000.000000000000000 ) ;
#2564=ORIENTED_EDGE ( 'NONE', *, *, #9879, .T. ) ;
#2594=ORIENTED_EDGE ( 'NONE', *, *, #905, .T. ) ;
#2632=ADVANCED_FACE ( 'NONE', ( #11802 ), #9718, .F. ) ;
#2639=DIRECTION ( 'NONE',  ( 0.000000000000000000, 0.000000000000000000, -1.000000000000000000 ) ) ;
#2693=ORIENTED_EDGE ( 'NONE', *, *, #8703, .T. ) ;
#2698=ADVANCED_FACE ( 'NONE', ( #11744 ), #1901, .T. ) ;
#2744=DIRECTION ( 'NONE',  ( 0.000000000000000000, 0.000000000000000000, 1.000000000000000000 ) ) ;
#2745=CARTESIAN_POINT ( 'NONE',  ( 11.99999999999999822, 9.000000000000000000, 0.000000000000000000 ) ) ;
#2755=VERTEX_POINT ( 'NONE', #4124 ) ;
#2762=LINE ( 'NONE', #736, #1793 ) ;
#2795=VERTEX_POINT ( 'NONE', #267 ) ;
#2797=DIRECTION ( 'NONE',  ( -1.000000000000000000, -0.000000000000000000, -0.000000000000000000 ) ) ;
#2803=CARTESIAN_POINT ( 'NONE',  ( 11.99999999999999645, 0.000000000000000000, 9.000000000000000000 ) ) ;
#2824=VECTOR ( 'NONE', #4395, 999.9999999999998863 ) ;
#2831=VERTEX_POINT ( 'NONE', #9206 ) ;
#2847=LINE ( 'NONE', #6709, #6692 ) ;
#2856=AXIS2_PLACEMENT_3D ( 'NONE', #3907, #936, #1876 ) ;
#2866=ORIENTED_EDGE ( 'NONE', *, *, #5273, .F. ) ;
#2888=CARTESIAN_POINT ( 'NONE',  ( 31.03600000000003689, 0.000000000000000000, 0.000000000000000000 ) ) ;
#2899=VERTEX_POINT ( 'NONE', #3669 ) ;
#2901=AXIS2_PLACEMENT_3D ( 'NONE', #6216, #324, #10089 ) ;
#2922=VERTEX_POINT ( 'NONE', #6467 ) ;
#2923=CARTESIAN_POINT ( 'NONE',  ( 6.000000000000000000, 8.759846959279592227, -5.057500000000009877 ) ) ;
#2950=DIRECTION ( 'NONE',  ( 0.000000000000000000, 0.000000000000000000, -1.000000000000000000 ) ) ;
#2970=DIRECTION ( 'NONE',  ( 1.000000000000000000, 0.000000000000000000, 0.000000000000000000 ) ) ;
#2990=LINE ( 'NONE', #10656, #1645 ) ;
#2991=ORIENTED_EDGE ( 'NONE', *, *, #2079, .F. ) ;
#3004=VERTEX_POINT ( 'NONE', #10211 ) ;
#3007=CARTESIAN_POINT ( 'NONE',  ( 0.6000000000000033085, 0.000000000000000000, 9.000000000000000000 ) ) ;
#3014=DIRECTION ( 'NONE',  ( 0.000000000000000000, 0.000000000000000000, 1.000000000000000000 ) ) ;
#3037=EDGE_CURVE ( 'NONE', #2485, #2795, #3484, .T. ) ;
#3042=EDGE_CURVE ( 'NONE', #2279, #12065, #11152, .T. ) ;
#3050=ORIENTED_EDGE ( 'NONE', *, *, #3042, .T. ) ;
#3051=DIRECTION ( 'NONE',  ( 0.000000000000000000, 0.000000000000000000, 1.000000000000000000 ) ) ;
#3064=FACE_OUTER_BOUND ( 'NONE', #8000, .T. ) ;
#3094=AXIS2_PLACEMENT_3D ( 'NONE', #12494, #3798, #3610 ) ;
#3135=VECTOR ( 'NONE', #5382, 999.9999999999998863 ) ;
#3142=ORIENTED_EDGE ( 'NONE', *, *, #12274, .T. ) ;
#3183=LINE ( 'NONE', #3874, #5294 ) ;
#3188=DIRECTION ( 'NONE',  ( -1.000000000000000000, -0.000000000000000000, -0.000000000000000000 ) ) ;
#3207=EDGE_CURVE ( 'NONE', #8345, #1560, #2847, .T. ) ;
#3231=ADVANCED_FACE ( 'NONE', ( #5136 ), #6271, .T. ) ;
#3244=ORIENTED_EDGE ( 'NONE', *, *, #2314, .F. ) ;
#3263=PLANE ( 'NONE',  #8460 ) ;
#3335=EDGE_CURVE ( 'NONE', #2279, #3004, #10902, .T. ) ;
#3352=ADVANCED_FACE ( 'NONE', ( #1747 ), #11341, .T. ) ;
#3370=SHAPE_REPRESENTATION ( 'socket head cap screw_iso_ISO 4762 M12 x 20 - 20N', ( #9021 ), #708 ) ;
#3403=CARTESIAN_POINT ( 'NONE',  ( 6.000000000000000000, -5.839897972853063557, 6.938893903907228378E-15 ) ) ;
#3430=( NAMED_UNIT ( * ) PLANE_ANGLE_UNIT ( ) SI_UNIT ( $, .RADIAN. ) );
#3456=LINE ( 'NONE', #9110, #6373 ) ;
#3470=CARTESIAN_POINT ( 'NONE',  ( 6.000000000000000000, 4.379923479639795225, -2.528750000000006271 ) ) ;
#3475=EDGE_LOOP ( 'NONE', ( #3637, #4801, #3531, #2066 ) ) ;
#3484=LINE ( 'NONE', #7354, #7915 ) ;
#3487=ADVANCED_FACE ( 'NONE', ( #10501 ), #8547, .T. ) ;
#3499=ORIENTED_EDGE ( 'NONE', *, *, #12097, .F. ) ;
#3501=ORIENTED_EDGE ( 'NONE', *, *, #10069, .F. ) ;
#3513=ORIENTED_EDGE ( 'NONE', *, *, #1524, .T. ) ;
#3515=DIRECTION ( 'NONE',  ( -1.000000000000000000, -0.000000000000000000, -0.000000000000000000 ) ) ;
#3516=ORIENTED_EDGE ( 'NONE', *, *, #6821, .T. ) ;
#3531=ORIENTED_EDGE ( 'NONE', *, *, #10882, .T. ) ;
#3535=EDGE_CURVE ( 'NONE', #5337, #2279, #7517, .T. ) ;
#3547=ORIENTED_EDGE ( 'NONE', *, *, #4033, .F. ) ;
#3599=CARTESIAN_POINT ( 'NONE',  ( 0.000000000000000000, 5.839897972853065333, -6.938893903907228378E-15 ) ) ;
#3607=FACE_BOUND ( 'NONE', #11949, .T. ) ;
#3610=DIRECTION ( 'NONE',  ( 0.000000000000000000, 0.000000000000000000, -1.000000000000000000 ) ) ;
#3637=ORIENTED_EDGE ( 'NONE', *, *, #2298, .F. ) ;
#3639=EDGE_LOOP ( 'NONE', ( #921, #9880, #2866, #836 ) ) ;
#3653=CARTESIAN_POINT ( 'NONE',  ( 6.000000000000000000, -5.839897972853063557, 6.938893903907228378E-15 ) ) ;
#3669=CARTESIAN_POINT ( 'NONE',  ( 8.919948986426568638, 0.000000000000000000, 0.000000000000000000 ) ) ;
#3696=AXIS2_PLACEMENT_3D ( 'NONE', #8258, #8137, #10164 ) ;
#3701=EDGE_LOOP ( 'NONE', ( #1143, #7125, #4972, #3499, #7374 ) ) ;
#3702=PLANE ( 'NONE',  #9711 ) ;
#3704=PLANE ( 'NONE',  #7398 ) ;
#3708=LINE ( 'NONE', #7591, #9421 ) ;
#3709=CARTESIAN_POINT ( 'NONE',  ( 12.59999999999999964, 0.000000000000000000, 0.000000000000000000 ) ) ;
#3720=DIRECTION ( 'NONE',  ( 0.000000000000000000, 0.000000000000000000, -1.000000000000000000 ) ) ;
#3750=LINE ( 'NONE', #11495, #2184 ) ;
#3773=DIRECTION ( 'NONE',  ( -1.000000000000000000, -0.000000000000000000, -0.000000000000000000 ) ) ;
#3780=VECTOR ( 'NONE', #4999, 999.9999999999998863 ) ;
#3788=DIRECTION ( 'NONE',  ( -1.000000000000000000, -0.000000000000000000, -0.000000000000000000 ) ) ;
#3789=EDGE_CURVE ( 'NONE', #2899, #5337, #2990, .T. ) ;
#3798=DIRECTION ( 'NONE',  ( 1.000000000000000000, 0.000000000000000000, 0.000000000000000000 ) ) ;
#3819=CARTESIAN_POINT ( 'NONE',  ( 32.00000000000000000, 0.000000000000000000, 5.035999999999999588 ) ) ;
#3850=VECTOR ( 'NONE', #9098, 1000.000000000000114 ) ;
#3853=EDGE_CURVE ( 'NONE', #10915, #10888, #3183, .T. ) ;
#3862=UNCERTAINTY_MEASURE_WITH_UNIT (LENGTH_MEASURE( 1.000000000000000082E-05 ), #7814, 'distance_accuracy_value', 'NONE');
#3871=EDGE_CURVE ( 'NONE', #12073, #10081, #10747, .T. ) ;
#3874=CARTESIAN_POINT ( 'NONE',  ( 0.000000000000000000, 2.919948986426526005, -5.057500000000003659 ) ) ;
#3889=CARTESIAN_POINT ( 'NONE',  ( 0.000000000000000000, 1.065442715258197248E-15, -8.400000000000000355 ) ) ;
#3893=FACE_OUTER_BOUND ( 'NONE', #8081, .T. ) ;
#3904=EDGE_LOOP ( 'NONE', ( #9429, #6032, #7106, #10703, #7655 ) ) ;
#3907=CARTESIAN_POINT ( 'NONE',  ( 6.000000000000000000, 0.000000000000000000, 0.000000000000000000 ) ) ;
#3942=DIRECTION ( 'NONE',  ( -1.000000000000000000, -0.000000000000000000, -0.000000000000000000 ) ) ;
#3946=DIRECTION ( 'NONE',  ( -0.7071067811865331398, 0.000000000000000000, 0.7071067811865617836 ) ) ;
#3998=ORIENTED_EDGE ( 'NONE', *, *, #11974, .T. ) ;
#4033=EDGE_CURVE ( 'NONE', #8859, #8129, #826, .T. ) ;
#4070=LINE ( 'NONE', #399, #11662 ) ;
#4078=ORIENTED_EDGE ( 'NONE', *, *, #6365, .T. ) ;
#4101=ADVANCED_FACE ( 'NONE', ( #11415 ), #7524, .F. ) ;
#4109=AXIS2_PLACEMENT_3D ( 'NONE', #5343, #459, #12128 ) ;
#4124=CARTESIAN_POINT ( 'NONE',  ( 6.000000000000000000, -5.258101095580057891E-15, -5.057500000000000107 ) ) ;
#4240=FACE_OUTER_BOUND ( 'NONE', #3701, .T. ) ;
#4265=ADVANCED_FACE ( 'NONE', ( #3607, #7485 ), #127, .T. ) ;
#4335=CARTESIAN_POINT ( 'NONE',  ( 0.000000000000000000, 5.839897972853065333, -6.938893903907228378E-15 ) ) ;
#4336=EDGE_CURVE ( 'NONE', #9180, #8859, #5076, .T. ) ;
#4338=DIRECTION ( 'NONE',  ( 0.000000000000000000, 0.000000000000000000, -1.000000000000000000 ) ) ;
#4368=DIRECTION ( 'NONE',  ( 1.000000000000000000, 0.000000000000000000, 0.000000000000000000 ) ) ;
#4381=CYLINDRICAL_SURFACE ( 'NONE', #3696, 9.000000000000000000 ) ;
#4387=ORIENTED_EDGE ( 'NONE', *, *, #9879, .F. ) ;
#4395=DIRECTION ( 'NONE',  ( 0.000000000000000000, -0.4999999999999989453, 0.8660254037844393737 ) ) ;
#4398=CIRCLE ( 'NONE', #954, 5.057500000000000107 ) ;
#4422=ORIENTED_EDGE ( 'NONE', *, *, #1524, .F. ) ;
#4440=CARTESIAN_POINT ( 'NONE',  ( 0.6000000000000033085, 0.000000000000000000, 8.400000000000000355 ) ) ;
#4460=DIRECTION ( 'NONE',  ( 1.000000000000000000, 0.000000000000000000, 0.000000000000000000 ) ) ;
#4473=ORIENTED_EDGE ( 'NONE', *, *, #11166, .F. ) ;
#4482=LINE ( 'NONE', #2389, #7058 ) ;
#4483=CARTESIAN_POINT ( 'NONE',  ( 6.000000000000000000, 5.839897972853065333, -6.938893903907228378E-15 ) ) ;
#4509=EDGE_CURVE ( 'NONE', #10081, #12073, #8074, .T. ) ;
#4529=EDGE_LOOP ( 'NONE', ( #10358, #4624, #6618 ) ) ;
#4544=DIRECTION ( 'NONE',  ( 0.000000000000000000, 0.000000000000000000, -1.000000000000000000 ) ) ;
#4580=ORIENTED_EDGE ( 'NONE', *, *, #6365, .F. ) ;
#4590=CIRCLE ( 'NONE', #6213, 8.400000000000000355 ) ;
#4602=DIRECTION ( 'NONE',  ( 0.000000000000000000, 0.4999999999999987232, -0.8660254037844393737 ) ) ;
#4623=DIRECTION ( 'NONE',  ( -1.000000000000000000, -0.000000000000000000, -0.000000000000000000 ) ) ;
#4624=ORIENTED_EDGE ( 'NONE', *, *, #11327, .T. ) ;
#4667=FACE_OUTER_BOUND ( 'NONE', #4529, .T. ) ;
#4676=DIRECTION ( 'NONE',  ( 0.000000000000000000, -0.4999999999999989453, 0.8660254037844393737 ) ) ;
#4707=FACE_OUTER_BOUND ( 'NONE', #3904, .T. ) ;
#4731=DIRECTION ( 'NONE',  ( 0.000000000000000000, -0.5000000000000011102, -0.8660254037844380415 ) ) ;
#4744=CARTESIAN_POINT ( 'NONE',  ( 6.000000000000000000, 0.000000000000000000, 0.000000000000000000 ) ) ;
#4756=AXIS2_PLACEMENT_3D ( 'NONE', #12104, #6326, #6264 ) ;
#4801=ORIENTED_EDGE ( 'NONE', *, *, #6893, .F. ) ;
#4809=CARTESIAN_POINT ( 'NONE',  ( 0.6000000000000033085, 0.000000000000000000, 0.000000000000000000 ) ) ;
#4812=VECTOR ( 'NONE', #11931, 1000.000000000000000 ) ;
#4814=DIRECTION ( 'NONE',  ( 0.000000000000000000, -0.4999999999999989453, 0.8660254037844393737 ) ) ;
#4817=DIRECTION ( 'NONE',  ( 0.000000000000000000, -0.5000000000000011102, -0.8660254037844380415 ) ) ;
#4831=ORIENTED_EDGE ( 'NONE', *, *, #3335, .T. ) ;
#4837=VECTOR ( 'NONE', #1505, 1000.000000000000000 ) ;
#4863=CARTESIAN_POINT ( 'NONE',  ( 31.03600000000003689, 7.347880794884123680E-16, -6.000000000000003553 ) ) ;
#4909=PLANE ( 'NONE',  #6443 ) ;
#4956=ORIENTED_EDGE ( 'NONE', *, *, #6821, .F. ) ;
#4969=CIRCLE ( 'NONE', #12064, 6.000000000000003553 ) ;
#4972=ORIENTED_EDGE ( 'NONE', *, *, #10366, .F. ) ;
#4977=ADVANCED_FACE ( 'NONE', ( #3064 ), #4909, .F. ) ;
#4999=DIRECTION ( 'NONE',  ( 0.000000000000000000, -0.5000000000000012212, -0.8660254037844380415 ) ) ;
#5002=DIRECTION ( 'NONE',  ( 0.000000000000000000, 0.000000000000000000, 1.000000000000000000 ) ) ;
#5007=ORIENTED_EDGE ( 'NONE', *, *, #3037, .T. ) ;
#5041=AXIS2_PLACEMENT_3D ( 'NONE', #1957, #191, #7798 ) ;
#5047=DIRECTION ( 'NONE',  ( 1.000000000000000000, 0.000000000000000000, 0.000000000000000000 ) ) ;
#5068=CARTESIAN_POINT ( 'NONE',  ( 6.000000000000000000, 8.759846959279592227, -5.057500000000009877 ) ) ;
#5076=LINE ( 'NONE', #7737, #12126 ) ;
#5100=ORIENTED_EDGE ( 'NONE', *, *, #4336, .T. ) ;
#5131=CARTESIAN_POINT ( 'NONE',  ( 0.000000000000000000, 0.000000000000000000, 0.000000000000000000 ) ) ;
#5136=FACE_OUTER_BOUND ( 'NONE', #8744, .T. ) ;
#5143=CIRCLE ( 'NONE', #2304, 6.000000000000003553 ) ;
#5166=VECTOR ( 'NONE', #3773, 1000.000000000000000 ) ;
#5186=AXIS2_PLACEMENT_3D ( 'NONE', #1448, #371, #7396 ) ;
#5192=( LENGTH_UNIT ( ) NAMED_UNIT ( * ) SI_UNIT ( .MILLI., .METRE. ) );
#5248=CARTESIAN_POINT ( 'NONE',  ( 0.000000000000000000, -5.839897972853063557, 6.938893903907228378E-15 ) ) ;
#5257=DIRECTION ( 'NONE',  ( 0.000000000000000000, 0.8660254037844379305, -0.5000000000000012212 ) ) ;
#5272=ORIENTED_EDGE ( 'NONE', *, *, #4336, .F. ) ;
#5273=EDGE_CURVE ( 'NONE', #1223, #2922, #8281, .T. ) ;
#5294=VECTOR ( 'NONE', #9720, 1000.000000000000000 ) ;
#5311=ORIENTED_EDGE ( 'NONE', *, *, #2346, .F. ) ;
#5312=EDGE_CURVE ( 'NONE', #11275, #2279, #8492, .T. ) ;
#5326=FACE_OUTER_BOUND ( 'NONE', #3475, .T. ) ;
#5337=VERTEX_POINT ( 'NONE', #1820 ) ;
#5343=CARTESIAN_POINT ( 'NONE',  ( 6.000000000000000000, 8.759846959279592227, -5.057500000000009877 ) ) ;
#5376=ADVANCED_FACE ( 'NONE', ( #1013 ), #2210, .F. ) ;
#5378=( NAMED_UNIT ( * ) SI_UNIT ( $, .STERADIAN. ) SOLID_ANGLE_UNIT ( ) );
#5381=VECTOR ( 'NONE', #7475, 999.9999999999998863 ) ;
#5382=DIRECTION ( 'NONE',  ( 0.000000000000000000, -0.5000000000000012212, -0.8660254037844380415 ) ) ;
#5415=STYLED_ITEM('',(#12591),#10384);
#5461=APPLICATION_CONTEXT ( 'automotive_design' ) ;
#5466=CARTESIAN_POINT ( 'NONE',  ( 6.000000000000000000, 0.000000000000000000, 0.000000000000000000 ) ) ;
#5526=EDGE_CURVE ( 'NONE', #11275, #1359, #4482, .T. ) ;
#5547=LINE ( 'NONE', #4335, #2824 ) ;
#5601=EDGE_CURVE ( 'NONE', #10486, #2485, #8356, .T. ) ;
#5629=CARTESIAN_POINT ( 'NONE',  ( 0.000000000000000000, 5.839897972853065333, -6.938893903907228378E-15 ) ) ;
#5651=FACE_OUTER_BOUND ( 'NONE', #3639, .T. ) ;
#5690=EDGE_CURVE ( 'NONE', #2755, #2795, #2762, .T. ) ;
#5711=ORIENTED_EDGE ( 'NONE', *, *, #10921, .F. ) ;
#5733=CARTESIAN_POINT ( 'NONE',  ( 6.000000000000000000, -5.839897972853063557, 6.938893903907228378E-15 ) ) ;
#5747=VECTOR ( 'NONE', #121, 1000.000000000000000 ) ;
#5755=EDGE_LOOP ( 'NONE', ( #4580, #5711, #47, #2015 ) ) ;
#5767=CIRCLE ( 'NONE', #8205, 8.400000000000000355 ) ;
#5785=DIRECTION ( 'NONE',  ( -1.000000000000000000, -0.000000000000000000, -0.000000000000000000 ) ) ;
#5787=DIRECTION ( 'NONE',  ( -1.000000000000000000, -0.000000000000000000, -0.000000000000000000 ) ) ;
#5863=ORIENTED_EDGE ( 'NONE', *, *, #2414, .T. ) ;
#5879=ORIENTED_EDGE ( 'NONE', *, *, #8703, .F. ) ;
#5894=DIRECTION ( 'NONE',  ( -1.000000000000000000, -0.000000000000000000, -0.000000000000000000 ) ) ;
#5943=ORIENTED_EDGE ( 'NONE', *, *, #7862, .F. ) ;
#6008=ORIENTED_EDGE ( 'NONE', *, *, #8425, .T. ) ;
#6016=CARTESIAN_POINT ( 'NONE',  ( 0.000000000000000000, 2.919948986426539772, 5.057499999999996554 ) ) ;
#6024=AXIS2_PLACEMENT_3D ( 'NONE', #4809, #8677, #8783 ) ;
#6032=ORIENTED_EDGE ( 'NONE', *, *, #11173, .F. ) ;
#6035=ORIENTED_EDGE ( 'NONE', *, *, #10610, .F. ) ;
#6082=DIRECTION ( 'NONE',  ( 0.000000000000000000, 0.000000000000000000, -1.000000000000000000 ) ) ;
#6087=DIRECTION ( 'NONE',  ( -1.000000000000000000, -0.000000000000000000, -0.000000000000000000 ) ) ;
#6146=AXIS2_PLACEMENT_3D ( 'NONE', #8009, #10859, #7048 ) ;
#6156=LINE ( 'NONE', #8062, #4812 ) ;
#6213=AXIS2_PLACEMENT_3D ( 'NONE', #507, #9262, #6275 ) ;
#6216=CARTESIAN_POINT ( 'NONE',  ( 11.99999999999999645, 0.000000000000000000, 0.000000000000000000 ) ) ;
#6225=( GEOMETRIC_REPRESENTATION_CONTEXT ( 3 ) GLOBAL_UNCERTAINTY_ASSIGNED_CONTEXT ( ( #7722 ) ) GLOBAL_UNIT_ASSIGNED_CONTEXT ( ( #5192, #11020, #5378 ) ) REPRESENTATION_CONTEXT ( 'NONE', 'WORKASPACE' ) );
#6255=ORIENTED_EDGE ( 'NONE', *, *, #4509, .F. ) ;
#6264=DIRECTION ( 'NONE',  ( 0.000000000000000000, 0.4999999999999988898, -0.8660254037844392627 ) ) ;
#6271=CYLINDRICAL_SURFACE ( 'NONE', #425, 9.000000000000000000 ) ;
#6275=DIRECTION ( 'NONE',  ( 0.000000000000000000, 0.000000000000000000, 1.000000000000000000 ) ) ;
#6287=DIRECTION ( 'NONE',  ( 0.000000000000000000, -1.000000000000000000, 0.000000000000000000 ) ) ;
#6302=ORIENTED_EDGE ( 'NONE', *, *, #5312, .T. ) ;
#6322=DIRECTION ( 'NONE',  ( -1.000000000000000000, -0.000000000000000000, -0.000000000000000000 ) ) ;
#6326=DIRECTION ( 'NONE',  ( 0.000000000000000000, -0.8660254037844392627, -0.4999999999999988898 ) ) ;
#6349=CIRCLE ( 'NONE', #478, 6.000000000000003553 ) ;
#6365=EDGE_CURVE ( 'NONE', #9622, #2202, #9308, .T. ) ;
#6373=VECTOR ( 'NONE', #2377, 1000.000000000000000 ) ;
#6388=CIRCLE ( 'NONE', #5186, 9.000000000000000000 ) ;
#6405=DIRECTION ( 'NONE',  ( 0.000000000000000000, 0.000000000000000000, 1.000000000000000000 ) ) ;
#6443=AXIS2_PLACEMENT_3D ( 'NONE', #979, #7886, #10793 ) ;
#6467=CARTESIAN_POINT ( 'NONE',  ( 12.00000000000000000, 8.082668874372534964E-16, 6.600000000000003197 ) ) ;
#6492=DIRECTION ( 'NONE',  ( -0.000000000000000000, 1.336710962791342904E-15, 1.000000000000000000 ) ) ;
#6505=DIRECTION ( 'NONE',  ( 0.000000000000000000, -1.000000000000000000, 1.039664082171044481E-15 ) ) ;
#6552=FACE_OUTER_BOUND ( 'NONE', #9303, .T. ) ;
#6569=DIRECTION ( 'NONE',  ( 1.000000000000000000, 0.000000000000000000, 0.000000000000000000 ) ) ;
#6573=DIRECTION ( 'NONE',  ( -0.000000000000000000, 0.8660254037844393737, 0.4999999999999987232 ) ) ;
#6574=VERTEX_POINT ( 'NONE', #6016 ) ;
#6577=ADVANCED_FACE ( 'NONE', ( #7857 ), #11207, .T. ) ;
#6603=DIRECTION ( 'NONE',  ( 0.000000000000000000, 0.000000000000000000, -1.000000000000000000 ) ) ;
#6618=ORIENTED_EDGE ( 'NONE', *, *, #905, .F. ) ;
#6630=DIRECTION ( 'NONE',  ( 0.000000000000000000, 0.000000000000000000, 1.000000000000000000 ) ) ;
#6632=ORIENTED_EDGE ( 'NONE', *, *, #2079, .T. ) ;
#6658=EDGE_CURVE ( 'NONE', #801, #2755, #11853, .T. ) ;
#6665=CIRCLE ( 'NONE', #10315, 6.600000000000003197 ) ;
#6692=VECTOR ( 'NONE', #4817, 1000.000000000000114 ) ;
#6709=CARTESIAN_POINT ( 'NONE',  ( 0.000000000000000000, -2.919948986426525117, 5.057500000000004547 ) ) ;
#6727=FACE_BOUND ( 'NONE', #11523, .T. ) ;
#6745=EDGE_LOOP ( 'NONE', ( #9566, #11179, #2146 ) ) ;
#6746=DIRECTION ( 'NONE',  ( 1.000000000000000000, 0.000000000000000000, 0.000000000000000000 ) ) ;
#6821=EDGE_CURVE ( 'NONE', #12014, #1979, #5143, .T. ) ;
#6825=FACE_OUTER_BOUND ( 'NONE', #934, .T. ) ;
#6876=EDGE_CURVE ( 'NONE', #1979, #7598, #932, .T. ) ;
#6893=EDGE_CURVE ( 'NONE', #7598, #8987, #6349, .T. ) ;
#6904=LINE ( 'NONE', #10770, #2558 ) ;
#6916=ORIENTED_EDGE ( 'NONE', *, *, #3335, .F. ) ;
#6930=ORIENTED_EDGE ( 'NONE', *, *, #10069, .T. ) ;
#6957=CIRCLE ( 'NONE', #885, 6.000000000000003553 ) ;
#6983=ADVANCED_FACE ( 'NONE', ( #7528 ), #108, .T. ) ;
#7003=CIRCLE ( 'NONE', #7207, 9.000000000000000000 ) ;
#7010=CARTESIAN_POINT ( 'NONE',  ( 6.000000000000000000, -2.919948986426538884, -5.057499999999997442 ) ) ;
#7026=DIRECTION ( 'NONE',  ( 0.000000000000000000, 0.5000000000000012212, 0.8660254037844379305 ) ) ;
#7040=ORIENTED_EDGE ( 'NONE', *, *, #5312, .F. ) ;
#7048=DIRECTION ( 'NONE',  ( 0.000000000000000000, 0.000000000000000000, 1.000000000000000000 ) ) ;
#7058=VECTOR ( 'NONE', #10195, 1000.000000000000000 ) ;
#7092=CIRCLE ( 'NONE', #9730, 5.057500000000000107 ) ;
#7105=ORIENTED_EDGE ( 'NONE', *, *, #3037, .F. ) ;
#7106=ORIENTED_EDGE ( 'NONE', *, *, #5690, .F. ) ;
#7125=ORIENTED_EDGE ( 'NONE', *, *, #8549, .F. ) ;
#7137=CARTESIAN_POINT ( 'NONE',  ( 0.000000000000000000, -5.839897972853063557, 6.938893903907228378E-15 ) ) ;
#7206=PRODUCT_DEFINITION_SHAPE ( 'NONE', 'NONE',  #1691 ) ;
#7207=AXIS2_PLACEMENT_3D ( 'NONE', #8546, #12413, #6630 ) ;
#7208=CARTESIAN_POINT ( 'NONE',  ( 0.000000000000000000, -2.919948986426538884, -5.057499999999997442 ) ) ;
#7265=EDGE_CURVE ( 'NONE', #8987, #7598, #6957, .T. ) ;
#7308=CARTESIAN_POINT ( 'NONE',  ( 12.59999999999999964, 8.082668874372534964E-16, 6.600000000000003197 ) ) ;
#7311=EDGE_LOOP ( 'NONE', ( #7813, #2991, #11446, #9692, #895 ) ) ;
#7349=VECTOR ( 'NONE', #2539, 1000.000000000000114 ) ;
#7354=CARTESIAN_POINT ( 'NONE',  ( 6.000000000000000000, -5.839897972853063557, 6.938893903907228378E-15 ) ) ;
#7374=ORIENTED_EDGE ( 'NONE', *, *, #5526, .T. ) ;
#7388=ORIENTED_EDGE ( 'NONE', *, *, #3871, .T. ) ;
#7392=LINE ( 'NONE', #5248, #1180 ) ;
#7396=DIRECTION ( 'NONE',  ( 0.000000000000000000, 0.000000000000000000, 1.000000000000000000 ) ) ;
#7398=AXIS2_PLACEMENT_3D ( 'NONE', #7460, #10558, #2639 ) ;
#7434=CARTESIAN_POINT ( 'NONE',  ( 6.000000000000000000, 0.000000000000000000, 0.000000000000000000 ) ) ;
#7436=EDGE_LOOP ( 'NONE', ( #8729, #10872, #5100, #8405 ) ) ;
#7438=ORIENTED_EDGE ( 'NONE', *, *, #3535, .F. ) ;
#7460=CARTESIAN_POINT ( 'NONE',  ( 6.000000000000000000, 8.759846959279592227, -5.057500000000009877 ) ) ;
#7475=DIRECTION ( 'NONE',  ( 0.000000000000000000, -0.5000000000000012212, -0.8660254037844380415 ) ) ;
#7485=FACE_OUTER_BOUND ( 'NONE', #420, .T. ) ;
#7499=ORIENTED_EDGE ( 'NONE', *, *, #3853, .F. ) ;
#7517=CIRCLE ( 'NONE', #2856, 5.057500000000000107 ) ;
#7524=CONICAL_SURFACE ( 'NONE', #2048, 5.057500000000000107, 1.047197551196592302 ) ;
#7528=FACE_OUTER_BOUND ( 'NONE', #11539, .T. ) ;
#7575=ORIENTED_EDGE ( 'NONE', *, *, #3789, .F. ) ;
#7582=DIRECTION ( 'NONE',  ( 0.000000000000000000, 0.000000000000000000, -1.000000000000000000 ) ) ;
#7591=CARTESIAN_POINT ( 'NONE',  ( 6.000000000000000000, -2.919948986426525117, 5.057500000000004547 ) ) ;
#7598=VERTEX_POINT ( 'NONE', #10058 ) ;
#7605=CARTESIAN_POINT ( 'NONE',  ( 6.000000000000000000, 5.839897972853065333, -6.938893903907228378E-15 ) ) ;
#7646=TOROIDAL_SURFACE ( 'NONE', #6024, 8.400000000000000355, 0.5999999999999999778 ) ;
#7650=ORIENTED_EDGE ( 'NONE', *, *, #2314, .T. ) ;
#7655=ORIENTED_EDGE ( 'NONE', *, *, #8549, .T. ) ;
#7677=LINE ( 'NONE', #11359, #7349 ) ;
#7692=PLANE ( 'NONE',  #8304 ) ;
#7722=UNCERTAINTY_MEASURE_WITH_UNIT (LENGTH_MEASURE( 1.000000000000000082E-05 ), #5192, 'distance_accuracy_value', 'NONE');
#7737=CARTESIAN_POINT ( 'NONE',  ( -31.74999999999995737, 0.000000000000000000, 9.000000000000000000 ) ) ;
#7746=ORIENTED_EDGE ( 'NONE', *, *, #4509, .T. ) ;
#7747=CARTESIAN_POINT ( 'NONE',  ( -31.74999999999995737, 0.000000000000000000, 0.000000000000000000 ) ) ;
#7748=ORIENTED_EDGE ( 'NONE', *, *, #3535, .T. ) ;
#7770=CARTESIAN_POINT ( 'NONE',  ( 12.59999999999999964, 0.000000000000000000, 0.000000000000000000 ) ) ;
#7771=AXIS2_PLACEMENT_3D ( 'NONE', #2012, #1139, #8049 ) ;
#7790=CARTESIAN_POINT ( 'NONE',  ( 6.000000000000000000, 5.839897972853065333, -6.938893903907228378E-15 ) ) ;
#7798=DIRECTION ( 'NONE',  ( -0.000000000000000000, 0.000000000000000000, 1.000000000000000000 ) ) ;
#7813=ORIENTED_EDGE ( 'NONE', *, *, #3207, .F. ) ;
#7814=( LENGTH_UNIT ( ) NAMED_UNIT ( * ) SI_UNIT ( .MILLI., .METRE. ) );
#7857=FACE_OUTER_BOUND ( 'NONE', #7861, .T. ) ;
#7861=EDGE_LOOP ( 'NONE', ( #5311, #7746, #9412, #4473 ) ) ;
#7862=EDGE_CURVE ( 'NONE', #1674, #9180, #1879, .T. ) ;
#7873=ORIENTED_EDGE ( 'NONE', *, *, #12097, .T. ) ;
#7876=CARTESIAN_POINT ( 'NONE',  ( 32.00000000000000000, 0.000000000000000000, 0.000000000000000000 ) ) ;
#7886=DIRECTION ( 'NONE',  ( 1.000000000000000000, 0.000000000000000000, 0.000000000000000000 ) ) ;
#7915=VECTOR ( 'NONE', #757, 1000.000000000000000 ) ;
#7977=VECTOR ( 'NONE', #11338, 1000.000000000000000 ) ;
#8000=EDGE_LOOP ( 'NONE', ( #8901, #7105, #3501 ) ) ;
#8009=CARTESIAN_POINT ( 'NONE',  ( 11.99999999999999645, 0.000000000000000000, 0.000000000000000000 ) ) ;
#8014=ADVANCED_FACE ( 'NONE', ( #520 ), #4381, .T. ) ;
#8016=ORIENTED_EDGE ( 'NONE', *, *, #7265, .T. ) ;
#8024=AXIS2_PLACEMENT_3D ( 'NONE', #11588, #8730, #1000 ) ;
#8046=ADVANCED_FACE ( 'NONE', ( #10219 ), #11229, .F. ) ;
#8049=DIRECTION ( 'NONE',  ( 0.000000000000000000, 0.000000000000000000, 1.000000000000000000 ) ) ;
#8062=CARTESIAN_POINT ( 'NONE',  ( 6.000000000000000000, 2.919948986426526005, -5.057500000000003659 ) ) ;
#8074=CIRCLE ( 'NONE', #8878, 5.035999999999999588 ) ;
#8081=EDGE_LOOP ( 'NONE', ( #296, #6255 ) ) ;
#8101=CARTESIAN_POINT ( 'NONE',  ( 6.000000000000000000, 2.919948986426539772, 5.057499999999996554 ) ) ;
#8126=AXIS2_PLACEMENT_3D ( 'NONE', #5466, #4623, #6405 ) ;
#8129=VERTEX_POINT ( 'NONE', #12249 ) ;
#8137=DIRECTION ( 'NONE',  ( -1.000000000000000000, -0.000000000000000000, -0.000000000000000000 ) ) ;
#8168=ADVANCED_FACE ( 'NONE', ( #5651 ), #11202, .F. ) ;
#8193=DIRECTION ( 'NONE',  ( 0.000000000000000000, 0.000000000000000000, -1.000000000000000000 ) ) ;
#8205=AXIS2_PLACEMENT_3D ( 'NONE', #5131, #11852, #5002 ) ;
#8225=EDGE_CURVE ( 'NONE', #9848, #2831, #7677, .T. ) ;
#8256=VECTOR ( 'NONE', #3946, 1000.000000000000114 ) ;
#8258=CARTESIAN_POINT ( 'NONE',  ( -31.74999999999995737, 0.000000000000000000, 0.000000000000000000 ) ) ;
#8274=CARTESIAN_POINT ( 'NONE',  ( 12.59999999999999964, 0.000000000000000000, 6.000000000000003553 ) ) ;
#8281=CIRCLE ( 'NONE', #1589, 6.600000000000003197 ) ;
#8304=AXIS2_PLACEMENT_3D ( 'NONE', #2745, #11494, #6603 ) ;
#8345=VERTEX_POINT ( 'NONE', #10840 ) ;
#8352=CARTESIAN_POINT ( 'NONE',  ( 6.000000000000000000, 0.000000000000000000, 0.000000000000000000 ) ) ;
#8355=CARTESIAN_POINT ( 'NONE',  ( 0.000000000000000000, 2.919948986426526005, -5.057500000000003659 ) ) ;
#8356=LINE ( 'NONE', #3403, #4837 ) ;
#8405=ORIENTED_EDGE ( 'NONE', *, *, #10921, .T. ) ;
#8425=EDGE_CURVE ( 'NONE', #9180, #1674, #12219, .T. ) ;
#8433=CARTESIAN_POINT ( 'NONE',  ( 0.6000000000000033085, 1.028703311283776586E-15, -8.400000000000000355 ) ) ;
#8460=AXIS2_PLACEMENT_3D ( 'NONE', #9042, #4460, #4338 ) ;
#8471=EDGE_LOOP ( 'NONE', ( #10496, #11182, #10953 ) ) ;
#8492=LINE ( 'NONE', #7605, #12335 ) ;
#8496=CLOSED_SHELL ( 'NONE', ( #8694, #10180, #8168, #1330, #2698, #3231, #4265, #8014, #679, #6983, #6577, #255, #9484, #1300, #12038, #11492, #3487, #3352, #9135, #1004, #4977, #9003, #10959, #8046, #2632, #5376, #4101 ) ) ;
#8540=ADVANCED_BREP_SHAPE_REPRESENTATION ( '', ( #10384, #9021 ), #708 ) ;
#8546=CARTESIAN_POINT ( 'NONE',  ( 0.6000000000000033085, 0.000000000000000000, 0.000000000000000000 ) ) ;
#8547=PLANE ( 'NONE',  #634 ) ;
#8549=EDGE_CURVE ( 'NONE', #801, #10915, #6156, .T. ) ;
#8579=CARTESIAN_POINT ( 'NONE',  ( 6.000000000000000000, 2.919948986426526005, -5.057500000000003659 ) ) ;
#8584=PLANE ( 'NONE',  #9000 ) ;
#8590=ORIENTED_EDGE ( 'NONE', *, *, #5273, .T. ) ;
#8593=CARTESIAN_POINT ( 'NONE',  ( 11.99999999999999822, 0.000000000000000000, 0.000000000000000000 ) ) ;
#8605=CARTESIAN_POINT ( 'NONE',  ( 32.00000000000000000, 0.000000000000000000, 0.000000000000000000 ) ) ;
#8610=CARTESIAN_POINT ( 'NONE',  ( 0.6000000000000033085, 1.102182119232617714E-15, -9.000000000000000000 ) ) ;
#8637=AXIS2_PLACEMENT_3D ( 'NONE', #9850, #3942, #8706 ) ;
#8664=CARTESIAN_POINT ( 'NONE',  ( -31.74999999999995737, 7.347880794884123680E-16, -6.000000000000003553 ) ) ;
#8666=CIRCLE ( 'NONE', #8637, 5.057500000000000107 ) ;
#8677=DIRECTION ( 'NONE',  ( -1.000000000000000000, -0.000000000000000000, -0.000000000000000000 ) ) ;
#8694=ADVANCED_FACE ( 'NONE', ( #2446 ), #161, .F. ) ;
#8703=EDGE_CURVE ( 'NONE', #1560, #10888, #7392, .T. ) ;
#8706=DIRECTION ( 'NONE',  ( 0.000000000000000000, 0.000000000000000000, 1.000000000000000000 ) ) ;
#8729=ORIENTED_EDGE ( 'NONE', *, *, #2062, .F. ) ;
#8730=DIRECTION ( 'NONE',  ( -1.000000000000000000, -0.000000000000000000, -0.000000000000000000 ) ) ;
#8734=AXIS2_PLACEMENT_3D ( 'NONE', #7876, #5787, #1036 ) ;
#8744=EDGE_LOOP ( 'NONE', ( #6008, #11842, #10376, #5272 ) ) ;
#8753=ORIENTED_EDGE ( 'NONE', *, *, #10775, .F. ) ;
#8764=LINE ( 'NONE', #3819, #8256 ) ;
#8780=AXIS2_PLACEMENT_3D ( 'NONE', #170, #2060, #9687 ) ;
#8783=DIRECTION ( 'NONE',  ( 0.000000000000000000, 0.000000000000000000, 1.000000000000000000 ) ) ;
#8797=CARTESIAN_POINT ( 'NONE',  ( 6.000000000000000000, -2.919948986426525117, 5.057500000000004547 ) ) ;
#8819=DIRECTION ( 'NONE',  ( 0.000000000000000000, 0.000000000000000000, -1.000000000000000000 ) ) ;
#8859=VERTEX_POINT ( 'NONE', #3007 ) ;
#8869=CARTESIAN_POINT ( 'NONE',  ( 6.000000000000000000, 5.839897972853065333, -6.938893903907228378E-15 ) ) ;
#8878=AXIS2_PLACEMENT_3D ( 'NONE', #11648, #2193, #3014 ) ;
#8885=DIRECTION ( 'NONE',  ( 1.000000000000000000, 0.000000000000000000, 0.000000000000000000 ) ) ;
#8901=ORIENTED_EDGE ( 'NONE', *, *, #5690, .T. ) ;
#8912=LINE ( 'NONE', #7010, #1129 ) ;
#8942=AXIS2_PLACEMENT_3D ( 'NONE', #4440, #6287, #8193 ) ;
#8987=VERTEX_POINT ( 'NONE', #8274 ) ;
#9000=AXIS2_PLACEMENT_3D ( 'NONE', #1732, #6492, #10356 ) ;
#9003=ADVANCED_FACE ( 'NONE', ( #9167 ), #3263, .F. ) ;
#9021=AXIS2_PLACEMENT_3D ( 'NONE', #11433, #2744, #207 ) ;
#9024=CARTESIAN_POINT ( 'NONE',  ( 6.000000000000000000, 2.919948986426526005, -5.057500000000003659 ) ) ;
#9035=CARTESIAN_POINT ( 'NONE',  ( 6.000000000000000000, -2.919948986426525117, 5.057500000000004547 ) ) ;
#9042=CARTESIAN_POINT ( 'NONE',  ( 6.000000000000000000, 8.759846959279592227, -5.057500000000009877 ) ) ;
#9044=PRODUCT_DEFINITION_CONTEXT ( 'detailed design', #5461, 'design' ) ;
#9051=LINE ( 'NONE', #11135, #10106 ) ;
#9098=DIRECTION ( 'NONE',  ( -0.7071067811865331398, 8.659560562355109119E-17, -0.7071067811865617836 ) ) ;
#9110=CARTESIAN_POINT ( 'NONE',  ( 6.000000000000000000, -2.919948986426525117, 5.057500000000004547 ) ) ;
#9115=DIRECTION ( 'NONE',  ( -1.000000000000000000, -0.000000000000000000, -0.000000000000000000 ) ) ;
#9135=ADVANCED_FACE ( 'NONE', ( #4707 ), #1666, .F. ) ;
#9161=DIRECTION ( 'NONE',  ( 0.000000000000000000, 1.000000000000000000, -1.224646799147353207E-16 ) ) ;
#9167=FACE_OUTER_BOUND ( 'NONE', #8471, .T. ) ;
#9179=EDGE_CURVE ( 'NONE', #2899, #2755, #3750, .T. ) ;
#9180=VERTEX_POINT ( 'NONE', #2803 ) ;
#9206=CARTESIAN_POINT ( 'NONE',  ( 6.000000000000000000, -4.379923479639794337, 2.528750000000004938 ) ) ;
#9238=ORIENTED_EDGE ( 'NONE', *, *, #498, .F. ) ;
#9262=DIRECTION ( 'NONE',  ( -1.000000000000000000, -0.000000000000000000, -0.000000000000000000 ) ) ;
#9285=DIRECTION ( 'NONE',  ( 0.000000000000000000, 1.224646799147351728E-16, 1.000000000000000000 ) ) ;
#9303=EDGE_LOOP ( 'NONE', ( #2564, #4422, #3244, #9756, #6632 ) ) ;
#9308=CIRCLE ( 'NONE', #11622, 0.5999999999999998668 ) ;
#9329=EDGE_CURVE ( 'NONE', #2485, #2831, #8666, .T. ) ;
#9350=APPLICATION_CONTEXT ( 'automotive_design' ) ;
#9368=ORIENTED_EDGE ( 'NONE', *, *, #9935, .T. ) ;
#9398=PRODUCT_DEFINITION_FORMATION_WITH_SPECIFIED_SOURCE ( 'ANY', '', #8, .NOT_KNOWN. ) ;
#9412=ORIENTED_EDGE ( 'NONE', *, *, #10476, .T. ) ;
#9421=VECTOR ( 'NONE', #4731, 1000.000000000000114 ) ;
#9429=ORIENTED_EDGE ( 'NONE', *, *, #3853, .T. ) ;
#9436=CARTESIAN_POINT ( 'NONE',  ( -31.74999999999995737, 0.000000000000000000, 6.000000000000003553 ) ) ;
#9484=ADVANCED_FACE ( 'NONE', ( #5326 ), #10455, .F. ) ;
#9509=DIRECTION ( 'NONE',  ( 0.000000000000000000, 0.000000000000000000, 1.000000000000000000 ) ) ;
#9516=DIRECTION ( 'NONE',  ( 0.000000000000000000, 0.000000000000000000, 1.000000000000000000 ) ) ;
#9566=ORIENTED_EDGE ( 'NONE', *, *, #10366, .T. ) ;
#9578=DIRECTION ( 'NONE',  ( -1.000000000000000000, -0.000000000000000000, -0.000000000000000000 ) ) ;
#9613=CARTESIAN_POINT ( 'NONE',  ( 32.00000000000000000, 5.035999999999999588, 0.000000000000000000 ) ) ;
#9622=VERTEX_POINT ( 'NONE', #8610 ) ;
#9640=CIRCLE ( 'NONE', #11062, 5.057500000000000107 ) ;
#9644=CONICAL_SURFACE ( 'NONE', #10850, 5.035999999999999588, 0.7853981633974685961 ) ;
#9659=DIRECTION ( 'NONE',  ( -0.5000000000000046629, 0.000000000000000000, 0.8660254037844359321 ) ) ;
#9674=ORIENTED_EDGE ( 'NONE', *, *, #3042, .F. ) ;
#9676=DIRECTION ( 'NONE',  ( -1.000000000000000000, -0.000000000000000000, -0.000000000000000000 ) ) ;
#9687=DIRECTION ( 'NONE',  ( 0.000000000000000000, 0.000000000000000000, 1.000000000000000000 ) ) ;
#9692=ORIENTED_EDGE ( 'NONE', *, *, #12244, .T. ) ;
#9711=AXIS2_PLACEMENT_3D ( 'NONE', #9613, #6746, #7582 ) ;
#9718=PLANE ( 'NONE',  #2017 ) ;
#9720=DIRECTION ( 'NONE',  ( 0.000000000000000000, -1.000000000000000000, 1.039664082171044481E-15 ) ) ;
#9730=AXIS2_PLACEMENT_3D ( 'NONE', #7434, #2797, #11239 ) ;
#9756=ORIENTED_EDGE ( 'NONE', *, *, #11327, .F. ) ;
#9834=AXIS2_PLACEMENT_3D ( 'NONE', #552, #11203, #1504 ) ;
#9848=VERTEX_POINT ( 'NONE', #8797 ) ;
#9850=CARTESIAN_POINT ( 'NONE',  ( 6.000000000000000000, 0.000000000000000000, 0.000000000000000000 ) ) ;
#9879=EDGE_CURVE ( 'NONE', #8345, #6574, #6904, .T. ) ;
#9880=ORIENTED_EDGE ( 'NONE', *, *, #2298, .T. ) ;
#9908=ORIENTED_EDGE ( 'NONE', *, *, #11166, .T. ) ;
#9926=DIRECTION ( 'NONE',  ( 0.000000000000000000, 0.5000000000000011102, 0.8660254037844379305 ) ) ;
#9935=EDGE_CURVE ( 'NONE', #2202, #8129, #4590, .T. ) ;
#10003=CARTESIAN_POINT ( 'NONE',  ( -31.74999999999995737, 1.102182119232617714E-15, -9.000000000000000000 ) ) ;
#10021=CARTESIAN_POINT ( 'NONE',  ( -31.74999999999995737, 0.000000000000000000, 0.000000000000000000 ) ) ;
#10034=ORIENTED_EDGE ( 'NONE', *, *, #8425, .F. ) ;
#10039=ORIENTED_EDGE ( 'NONE', *, *, #3789, .T. ) ;
#10049=EDGE_LOOP ( 'NONE', ( #10034, #5943 ) ) ;
#10058=CARTESIAN_POINT ( 'NONE',  ( 12.59999999999999964, 7.347880794884123680E-16, -6.000000000000003553 ) ) ;
#10069=EDGE_CURVE ( 'NONE', #2755, #2485, #4398, .T. ) ;
#10072=DIRECTION ( 'NONE',  ( 0.000000000000000000, 0.000000000000000000, 1.000000000000000000 ) ) ;
#10081=VERTEX_POINT ( 'NONE', #11346 ) ;
#10089=DIRECTION ( 'NONE',  ( 0.000000000000000000, 0.000000000000000000, 1.000000000000000000 ) ) ;
#10106=VECTOR ( 'NONE', #3515, 1000.000000000000000 ) ;
#10138=AXIS2_PLACEMENT_3D ( 'NONE', #7747, #5785, #3051 ) ;
#10164=DIRECTION ( 'NONE',  ( 0.000000000000000000, 0.000000000000000000, 1.000000000000000000 ) ) ;
#10180=ADVANCED_FACE ( 'NONE', ( #1635 ), #7646, .T. ) ;
#10195=DIRECTION ( 'NONE',  ( -1.000000000000000000, -0.000000000000000000, -0.000000000000000000 ) ) ;
#10211=CARTESIAN_POINT ( 'NONE',  ( 6.000000000000000000, 2.919948986426539772, 5.057499999999996554 ) ) ;
#10219=FACE_OUTER_BOUND ( 'NONE', #11732, .T. ) ;
#10284=EDGE_LOOP ( 'NONE', ( #7040, #7873, #9674 ) ) ;
#10307=DIRECTION ( 'NONE',  ( -1.000000000000000000, -0.000000000000000000, -0.000000000000000000 ) ) ;
#10314=EDGE_LOOP ( 'NONE', ( #3516, #158, #1296, #12520 ) ) ;
#10315=AXIS2_PLACEMENT_3D ( 'NONE', #8593, #9676, #12463 ) ;
#10356=DIRECTION ( 'NONE',  ( 0.000000000000000000, -1.000000000000000000, 1.336710962791342904E-15 ) ) ;
#10358=ORIENTED_EDGE ( 'NONE', *, *, #8225, .F. ) ;
#10366=EDGE_CURVE ( 'NONE', #12065, #801, #245, .T. ) ;
#10376=ORIENTED_EDGE ( 'NONE', *, *, #1394, .T. ) ;
#10384=MANIFOLD_SOLID_BREP ( 'Hex', #8496 ) ;
#10455=TOROIDAL_SURFACE ( 'NONE', #10658, 6.600000000000003197, 0.5999999999999999778 ) ;
#10470=ORIENTED_EDGE ( 'NONE', *, *, #2346, .T. ) ;
#10476=EDGE_CURVE ( 'NONE', #12073, #12014, #8764, .T. ) ;
#10486=VERTEX_POINT ( 'NONE', #5733 ) ;
#10496=ORIENTED_EDGE ( 'NONE', *, *, #5601, .F. ) ;
#10501=FACE_OUTER_BOUND ( 'NONE', #7311, .T. ) ;
#10558=DIRECTION ( 'NONE',  ( 1.000000000000000000, 0.000000000000000000, 0.000000000000000000 ) ) ;
#10610=EDGE_CURVE ( 'NONE', #10486, #1560, #4070, .T. ) ;
#10644=SHAPE_DEFINITION_REPRESENTATION ( #7206, #3370 ) ;
#10656=CARTESIAN_POINT ( 'NONE',  ( 6.000000000000000000, 0.000000000000000000, 5.057500000000000107 ) ) ;
#10658=AXIS2_PLACEMENT_3D ( 'NONE', #505, #4368, #2523 ) ;
#10670=ORIENTED_EDGE ( 'NONE', *, *, #1394, .F. ) ;
#10700=CARTESIAN_POINT ( 'NONE',  ( 6.000000000000000000, 0.000000000000000000, 0.000000000000000000 ) ) ;
#10703=ORIENTED_EDGE ( 'NONE', *, *, #6658, .F. ) ;
#10736=ORIENTED_EDGE ( 'NONE', *, *, #5601, .T. ) ;
#10747=CIRCLE ( 'NONE', #8734, 5.035999999999999588 ) ;
#10770=CARTESIAN_POINT ( 'NONE',  ( 0.000000000000000000, -2.919948986426525117, 5.057500000000004547 ) ) ;
#10775=EDGE_CURVE ( 'NONE', #1359, #10915, #12300, .T. ) ;
#10793=DIRECTION ( 'NONE',  ( 0.000000000000000000, 0.000000000000000000, -1.000000000000000000 ) ) ;
#10827=FACE_OUTER_BOUND ( 'NONE', #10938, .T. ) ;
#10836=CIRCLE ( 'NONE', #9834, 0.5999999999999998668 ) ;
#10840=CARTESIAN_POINT ( 'NONE',  ( 0.000000000000000000, -2.919948986426525117, 5.057500000000004547 ) ) ;
#10850=AXIS2_PLACEMENT_3D ( 'NONE', #8605, #2000, #1812 ) ;
#10859=DIRECTION ( 'NONE',  ( -1.000000000000000000, -0.000000000000000000, -0.000000000000000000 ) ) ;
#10872=ORIENTED_EDGE ( 'NONE', *, *, #7862, .T. ) ;
#10882=EDGE_CURVE ( 'NONE', #7598, #1223, #10836, .T. ) ;
#10888=VERTEX_POINT ( 'NONE', #7208 ) ;
#10902=LINE ( 'NONE', #12229, #10962 ) ;
#10915=VERTEX_POINT ( 'NONE', #8355 ) ;
#10920=EDGE_LOOP ( 'NONE', ( #929, #10039, #7748, #3050, #5863 ) ) ;
#10921=EDGE_CURVE ( 'NONE', #8859, #9622, #6388, .T. ) ;
#10934=CARTESIAN_POINT ( 'NONE',  ( 6.000000000000000000, 4.379923479639802331, 2.528749999999995168 ) ) ;
#10938=EDGE_LOOP ( 'NONE', ( #9238, #11526, #6302, #4831, #3513 ) ) ;
#10953=ORIENTED_EDGE ( 'NONE', *, *, #9329, .F. ) ;
#10959=ADVANCED_FACE ( 'NONE', ( #4667 ), #3704, .F. ) ;
#10962=VECTOR ( 'NONE', #4676, 999.9999999999998863 ) ;
#10984=EDGE_LOOP ( 'NONE', ( #5879, #6035, #10736, #5007, #2096 ) ) ;
#11020=( NAMED_UNIT ( * ) PLANE_ANGLE_UNIT ( ) SI_UNIT ( $, .RADIAN. ) );
#11062=AXIS2_PLACEMENT_3D ( 'NONE', #10700, #5894, #9516 ) ;
#11135=CARTESIAN_POINT ( 'NONE',  ( 6.000000000000000000, -2.919948986426525117, 5.057500000000004547 ) ) ;
#11152=CIRCLE ( 'NONE', #8126, 5.057500000000000107 ) ;
#11166=EDGE_CURVE ( 'NONE', #1979, #12014, #4969, .T. ) ;
#11173=EDGE_CURVE ( 'NONE', #2795, #10888, #8912, .T. ) ;
#11179=ORIENTED_EDGE ( 'NONE', *, *, #6658, .T. ) ;
#11182=ORIENTED_EDGE ( 'NONE', *, *, #12244, .F. ) ;
#11202=TOROIDAL_SURFACE ( 'NONE', #3094, 6.600000000000003197, 0.5999999999999999778 ) ;
#11203=DIRECTION ( 'NONE',  ( 0.000000000000000000, -1.000000000000000000, 0.000000000000000000 ) ) ;
#11206=CARTESIAN_POINT ( 'NONE',  ( 12.00000000000000000, 0.000000000000000000, -6.600000000000003197 ) ) ;
#11207=CONICAL_SURFACE ( 'NONE', #7771, 5.035999999999999588, 0.7853981633974685961 ) ;
#11229=PLANE ( 'NONE',  #4109 ) ;
#11239=DIRECTION ( 'NONE',  ( 0.000000000000000000, 0.000000000000000000, 1.000000000000000000 ) ) ;
#11275=VERTEX_POINT ( 'NONE', #1435 ) ;
#11327=EDGE_CURVE ( 'NONE', #9848, #5337, #3456, .T. ) ;
#11338=DIRECTION ( 'NONE',  ( -1.000000000000000000, -0.000000000000000000, -0.000000000000000000 ) ) ;
#11341=PLANE ( 'NONE',  #15 ) ;
#11346=CARTESIAN_POINT ( 'NONE',  ( 32.00000000000000000, 6.757601037695096551E-16, -5.035999999999999588 ) ) ;
#11357=DIRECTION ( 'NONE',  ( 0.000000000000000000, 0.000000000000000000, 1.000000000000000000 ) ) ;
#11359=CARTESIAN_POINT ( 'NONE',  ( 6.000000000000000000, -2.919948986426525117, 5.057500000000004547 ) ) ;
#11399=ORIENTED_EDGE ( 'NONE', *, *, #10476, .F. ) ;
#11413=ORIENTED_EDGE ( 'NONE', *, *, #498, .T. ) ;
#11415=FACE_OUTER_BOUND ( 'NONE', #10920, .T. ) ;
#11433=CARTESIAN_POINT ( 'NONE',  ( 0.000000000000000000, 0.000000000000000000, 0.000000000000000000 ) ) ;
#11435=DIRECTION ( 'NONE',  ( 0.000000000000000000, -1.039664082171044481E-15, -1.000000000000000000 ) ) ;
#11446=ORIENTED_EDGE ( 'NONE', *, *, #8225, .T. ) ;
#11492=ADVANCED_FACE ( 'NONE', ( #6552 ), #8584, .F. ) ;
#11494=DIRECTION ( 'NONE',  ( 1.000000000000000000, 0.000000000000000000, 0.000000000000000000 ) ) ;
#11495=CARTESIAN_POINT ( 'NONE',  ( 6.000000000000000000, 6.193651186687738874E-16, -5.057500000000000107 ) ) ;
#11498=AXIS2_PLACEMENT_3D ( 'NONE', #8579, #11435, #12390 ) ;
#11523=EDGE_LOOP ( 'NONE', ( #8590, #278 ) ) ;
#11526=ORIENTED_EDGE ( 'NONE', *, *, #5526, .F. ) ;
#11539=EDGE_LOOP ( 'NONE', ( #2548, #9908, #3142, #8016 ) ) ;
#11550=CIRCLE ( 'NONE', #413, 0.5999999999999998668 ) ;
#11573=ORIENTED_EDGE ( 'NONE', *, *, #3207, .T. ) ;
#11588=CARTESIAN_POINT ( 'NONE',  ( 0.6000000000000033085, 0.000000000000000000, 0.000000000000000000 ) ) ;
#11622=AXIS2_PLACEMENT_3D ( 'NONE', #8433, #2406, #2465 ) ;
#11648=CARTESIAN_POINT ( 'NONE',  ( 32.00000000000000000, 0.000000000000000000, 0.000000000000000000 ) ) ;
#11656=CARTESIAN_POINT ( 'NONE',  ( 6.000000000000000000, -2.919948986426525117, 5.057500000000004547 ) ) ;
#11662=VECTOR ( 'NONE', #3188, 1000.000000000000000 ) ;
#11732=EDGE_LOOP ( 'NONE', ( #7650, #6916, #7438 ) ) ;
#11744=FACE_OUTER_BOUND ( 'NONE', #10314, .T. ) ;
#11802=FACE_OUTER_BOUND ( 'NONE', #10284, .T. ) ;
#11842=ORIENTED_EDGE ( 'NONE', *, *, #2062, .T. ) ;
#11852=DIRECTION ( 'NONE',  ( -1.000000000000000000, -0.000000000000000000, -0.000000000000000000 ) ) ;
#11853=LINE ( 'NONE', #1203, #5747 ) ;
#11868=TOROIDAL_SURFACE ( 'NONE', #8024, 8.400000000000000355, 0.5999999999999999778 ) ;
#11931=DIRECTION ( 'NONE',  ( -1.000000000000000000, -0.000000000000000000, -0.000000000000000000 ) ) ;
#11949=EDGE_LOOP ( 'NONE', ( #11413, #4387, #11573, #2693, #7499, #8753 ) ) ;
#11967=DIRECTION ( 'NONE',  ( -1.000000000000000000, -0.000000000000000000, -0.000000000000000000 ) ) ;
#11974=EDGE_CURVE ( 'NONE', #8129, #2202, #5767, .T. ) ;
#12014=VERTEX_POINT ( 'NONE', #248 ) ;
#12030=CARTESIAN_POINT ( 'NONE',  ( 11.99999999999999645, 1.102182119232617714E-15, -9.000000000000000000 ) ) ;
#12038=ADVANCED_FACE ( 'NONE', ( #10827 ), #2452, .T. ) ;
#12064=AXIS2_PLACEMENT_3D ( 'NONE', #2888, #10307, #1624 ) ;
#12065=VERTEX_POINT ( 'NONE', #3470 ) ;
#12073=VERTEX_POINT ( 'NONE', #12166 ) ;
#12097=EDGE_CURVE ( 'NONE', #11275, #12065, #2517, .T. ) ;
#12104=CARTESIAN_POINT ( 'NONE',  ( 6.000000000000000000, 5.839897972853065333, -6.938893903907228378E-15 ) ) ;
#12112=AXIS2_PLACEMENT_3D ( 'NONE', #8352, #6322, #10072 ) ;
#12126=VECTOR ( 'NONE', #2016, 1000.000000000000000 ) ;
#12128=DIRECTION ( 'NONE',  ( 0.000000000000000000, 0.000000000000000000, -1.000000000000000000 ) ) ;
#12153=LINE ( 'NONE', #10003, #12327 ) ;
#12166=CARTESIAN_POINT ( 'NONE',  ( 32.00000000000000000, 0.000000000000000000, 5.035999999999999588 ) ) ;
#12167=DIRECTION ( 'NONE',  ( 0.000000000000000000, 0.000000000000000000, 1.000000000000000000 ) ) ;
#12198=CARTESIAN_POINT ( 'NONE',  ( 6.000000000000000000, -4.379923479639802331, -2.528749999999993836 ) ) ;
#12219=CIRCLE ( 'NONE', #2901, 9.000000000000000000 ) ;
#12229=CARTESIAN_POINT ( 'NONE',  ( 6.000000000000000000, 5.839897972853065333, -6.938893903907228378E-15 ) ) ;
#12244=EDGE_CURVE ( 'NONE', #2831, #10486, #3708, .T. ) ;
#12249=CARTESIAN_POINT ( 'NONE',  ( 0.000000000000000000, 0.000000000000000000, 8.400000000000000355 ) ) ;
#12274=EDGE_CURVE ( 'NONE', #12014, #8987, #12471, .T. ) ;
#12300=LINE ( 'NONE', #3599, #5381 ) ;
#12327=VECTOR ( 'NONE', #9115, 1000.000000000000000 ) ;
#12335=VECTOR ( 'NONE', #4814, 999.9999999999998863 ) ;
#12390=DIRECTION ( 'NONE',  ( 0.000000000000000000, 1.000000000000000000, -1.039664082171044481E-15 ) ) ;
#12413=DIRECTION ( 'NONE',  ( 1.000000000000000000, 0.000000000000000000, 0.000000000000000000 ) ) ;
#12414=DIRECTION ( 'NONE',  ( 0.000000000000000000, 0.8660254037844380415, -0.5000000000000012212 ) ) ;
#12463=DIRECTION ( 'NONE',  ( 0.000000000000000000, 0.000000000000000000, -1.000000000000000000 ) ) ;
#12471=LINE ( 'NONE', #9436, #5166 ) ;
#12475=FACE_OUTER_BOUND ( 'NONE', #5755, .T. ) ;
#12492=MECHANICAL_DESIGN_GEOMETRIC_PRESENTATION_REPRESENTATION('',(#5415),#6225);
#12494=CARTESIAN_POINT ( 'NONE',  ( 12.59999999999999964, 0.000000000000000000, 0.000000000000000000 ) ) ;
#12520=ORIENTED_EDGE ( 'NONE', *, *, #12274, .F. ) ;
#12585=COLOUR_RGB('Black',0.12,0.14,0.17);
#12586=FILL_AREA_STYLE_COLOUR('',#12585);
#12587=FILL_AREA_STYLE('',(#12586));
#12588=SURFACE_STYLE_FILL_AREA(#12587);
#12589=SURFACE_SIDE_STYLE('',(#12588));
#12590=SURFACE_STYLE_USAGE(.BOTH.,#12589);
#12591=PRESENTATION_STYLE_ASSIGNMENT((#12590));
ENDSEC;
END-ISO-10303-21;
